ISO-10303-21;
HEADER;
/* Generated by software containing ST-Developer
 * from STEP Tools, Inc. (www.steptools.com) 
 */

FILE_DESCRIPTION(
/* description */ ('Timing belt drive module 2 mm Pitch Timing 20T-40T'),

/* implementation_level */ '2;1');

FILE_NAME(
/* name */ 'M4 clamp nut (1).step',
/* time_stamp */ '2026-10-28T03:25:12-07:00',
/* author */ (''),
/* organization */ (''),
/* preprocessor_version */ 'ST-DEVELOPER v20.2',
/* originating_system */ 'Autodesk Translation Framework v15.17.0.0',
/* authorisation */ '');

FILE_SCHEMA (('AUTOMOTIVE_DESIGN { 1 0 10303 214 3 1 1 }'));
ENDSEC;

DATA;
#10=MECHANICAL_DESIGN_GEOMETRIC_PRESENTATION_REPRESENTATION('',(#533),#17830);
#447=SHAPE_REPRESENTATION_RELATIONSHIP('SRR','None',#18017,#490);
#490=ADVANCED_BREP_SHAPE_REPRESENTATION('',(#591),#17792);
#533=STYLED_ITEM('',(#18324),#591);
#591=MANIFOLD_SOLID_BREP('Body1',#8990);
#693=FACE_BOUND('',#1656,.T.);
#694=FACE_BOUND('',#1658,.T.);
#833=PLANE('',#9760);
#834=PLANE('',#9761);
#1076=FACE_OUTER_BOUND('',#1653,.T.);
#1077=FACE_OUTER_BOUND('',#1654,.T.);
#1078=FACE_OUTER_BOUND('',#1655,.T.);
#1079=FACE_OUTER_BOUND('',#1657,.T.);
#1653=EDGE_LOOP('',(#6325,#6326,#6327,#6328));
#1654=EDGE_LOOP('',(#6329,#6330,#6331,#6332));
#1655=EDGE_LOOP('',(#6333));
#1656=EDGE_LOOP('',(#6334));
#1657=EDGE_LOOP('',(#6335));
#1658=EDGE_LOOP('',(#6336));
#2252=CIRCLE('',#9755,0.165);
#2253=CIRCLE('',#9756,0.165);
#2254=CIRCLE('',#9758,0.4);
#2255=CIRCLE('',#9759,0.4);
#2954=LINE('',#14463,#3432);
#2955=LINE('',#14469,#3433);
#3432=VECTOR('',#11453,0.165);
#3433=VECTOR('',#11460,0.4);
#3930=VERTEX_POINT('',#14460);
#3931=VERTEX_POINT('',#14462);
#3932=VERTEX_POINT('',#14466);
#3933=VERTEX_POINT('',#14468);
#4845=EDGE_CURVE('',#3930,#3930,#2252,.T.);
#4846=EDGE_CURVE('',#3930,#3931,#2954,.T.);
#4847=EDGE_CURVE('',#3931,#3931,#2253,.T.);
#4848=EDGE_CURVE('',#3932,#3932,#2254,.T.);
#4849=EDGE_CURVE('',#3932,#3933,#2955,.T.);
#4850=EDGE_CURVE('',#3933,#3933,#2255,.T.);
#6325=ORIENTED_EDGE('',*,*,#4845,.F.);
#6326=ORIENTED_EDGE('',*,*,#4846,.T.);
#6327=ORIENTED_EDGE('',*,*,#4847,.T.);
#6328=ORIENTED_EDGE('',*,*,#4846,.F.);
#6329=ORIENTED_EDGE('',*,*,#4848,.F.);
#6330=ORIENTED_EDGE('',*,*,#4849,.T.);
#6331=ORIENTED_EDGE('',*,*,#4850,.T.);
#6332=ORIENTED_EDGE('',*,*,#4849,.F.);
#6333=ORIENTED_EDGE('',*,*,#4848,.T.);
#6334=ORIENTED_EDGE('',*,*,#4845,.T.);
#6335=ORIENTED_EDGE('',*,*,#4850,.F.);
#6336=ORIENTED_EDGE('',*,*,#4847,.F.);
#8235=CYLINDRICAL_SURFACE('',#9754,0.165);
#8236=CYLINDRICAL_SURFACE('',#9757,0.4);
#8574=ADVANCED_FACE('',(#1076),#8235,.F.);
#8575=ADVANCED_FACE('',(#1077),#8236,.T.);
#8576=ADVANCED_FACE('',(#1078,#693),#833,.T.);
#8577=ADVANCED_FACE('',(#1079,#694),#834,.F.);
#8990=CLOSED_SHELL('',(#8574,#8575,#8576,#8577));
#9753=AXIS2_PLACEMENT_3D('',#14458,#11447,#11448);
#9754=AXIS2_PLACEMENT_3D('',#14459,#11449,#11450);
#9755=AXIS2_PLACEMENT_3D('',#14461,#11451,#11452);
#9756=AXIS2_PLACEMENT_3D('',#14464,#11454,#11455);
#9757=AXIS2_PLACEMENT_3D('',#14465,#11456,#11457);
#9758=AXIS2_PLACEMENT_3D('',#14467,#11458,#11459);
#9759=AXIS2_PLACEMENT_3D('',#14470,#11461,#11462);
#9760=AXIS2_PLACEMENT_3D('',#14471,#11463,#11464);
#9761=AXIS2_PLACEMENT_3D('',#14472,#11465,#11466);
#11447=DIRECTION('axis',(0.,0.,1.));
#11448=DIRECTION('refdir',(1.,0.,0.));
#11449=DIRECTION('center_axis',(0.,0.,1.));
#11450=DIRECTION('ref_axis',(1.,0.,0.));
#11451=DIRECTION('center_axis',(0.,0.,-1.));
#11452=DIRECTION('ref_axis',(1.,0.,0.));
#11453=DIRECTION('',(0.,0.,-1.));
#11454=DIRECTION('center_axis',(0.,0.,-1.));
#11455=DIRECTION('ref_axis',(1.,0.,0.));
#11456=DIRECTION('center_axis',(0.,0.,1.));
#11457=DIRECTION('ref_axis',(1.,0.,0.));
#11458=DIRECTION('center_axis',(0.,0.,1.));
#11459=DIRECTION('ref_axis',(1.,0.,0.));
#11460=DIRECTION('',(0.,0.,-1.));
#11461=DIRECTION('center_axis',(0.,0.,1.));
#11462=DIRECTION('ref_axis',(1.,0.,0.));
#11463=DIRECTION('center_axis',(0.,0.,1.));
#11464=DIRECTION('ref_axis',(1.,0.,0.));
#11465=DIRECTION('center_axis',(0.,0.,1.));
#11466=DIRECTION('ref_axis',(1.,0.,0.));
#14458=CARTESIAN_POINT('',(0.,0.,0.));
#14459=CARTESIAN_POINT('Origin',(4.17091003018116,1.,-1.6));
#14460=CARTESIAN_POINT('',(4.00591003018116,1.,-1.2));
#14461=CARTESIAN_POINT('Origin',(4.17091003018116,1.,-1.2));
#14462=CARTESIAN_POINT('',(4.00591003018116,1.,-1.6));
#14463=CARTESIAN_POINT('',(4.00591003018116,1.,-1.6));
#14464=CARTESIAN_POINT('Origin',(4.17091003018116,1.,-1.6));
#14465=CARTESIAN_POINT('Origin',(4.17091003018116,1.,-1.6));
#14466=CARTESIAN_POINT('',(3.77091003018116,1.,-1.2));
#14467=CARTESIAN_POINT('Origin',(4.17091003018116,1.,-1.2));
#14468=CARTESIAN_POINT('',(3.77091003018116,1.,-1.6));
#14469=CARTESIAN_POINT('',(3.77091003018116,1.,-1.6));
#14470=CARTESIAN_POINT('Origin',(4.17091003018116,1.,-1.6));
#14471=CARTESIAN_POINT('Origin',(4.17091003018116,1.,-1.2));
#14472=CARTESIAN_POINT('Origin',(4.17091003018116,1.,-1.6));
#17742=UNCERTAINTY_MEASURE_WITH_UNIT(LENGTH_MEASURE(0.001),#17831,
'DISTANCE_ACCURACY_VALUE',
'Maximum model space distance between geometric entities at asserted c
onnectivities');
#17780=UNCERTAINTY_MEASURE_WITH_UNIT(LENGTH_MEASURE(0.001),#17831,
'DISTANCE_ACCURACY_VALUE',
'Maximum model space distance between geometric entities at asserted c
onnectivities');
#17792=(
GEOMETRIC_REPRESENTATION_CONTEXT(3)
GLOBAL_UNCERTAINTY_ASSIGNED_CONTEXT((#17742))
GLOBAL_UNIT_ASSIGNED_CONTEXT((#17831,#17833,#17834))
REPRESENTATION_CONTEXT('','3D')
);
#17830=(
GEOMETRIC_REPRESENTATION_CONTEXT(3)
GLOBAL_UNCERTAINTY_ASSIGNED_CONTEXT((#17780))
GLOBAL_UNIT_ASSIGNED_CONTEXT((#17831,#17833,#17834))
REPRESENTATION_CONTEXT('','3D')
);
#17831=(
LENGTH_UNIT()
NAMED_UNIT(*)
SI_UNIT(.CENTI.,.METRE.)
);
#17833=(
NAMED_UNIT(*)
PLANE_ANGLE_UNIT()
SI_UNIT($,.RADIAN.)
);
#17834=(
NAMED_UNIT(*)
SI_UNIT($,.STERADIAN.)
SOLID_ANGLE_UNIT()
);
#17846=SHAPE_DEFINITION_REPRESENTATION(#17895,#18017);
#17895=PRODUCT_DEFINITION_SHAPE('',$,#18067);
#18017=SHAPE_REPRESENTATION('',(#9753),#17792);
#18055=PRODUCT_DEFINITION_CONTEXT('part definition',#18204,'design');
#18067=PRODUCT_DEFINITION('M4 clamp nut (1)','M4 clamp nut (1)',#18116,#18055);
#18116=PRODUCT_DEFINITION_FORMATION('',$,#18217);
#18204=APPLICATION_CONTEXT(
'Core Data for Automotive Mechanical Design Process');
#18205=PRODUCT_CONTEXT('part definition',#18204,'mechanical');
#18217=PRODUCT('M4 clamp nut (1)','M4 clamp nut (1)','M4 clamp nut (1)',(#18205));
#18318=COLOUR_RGB('Black',0.12,0.14,0.17);
#18319=FILL_AREA_STYLE_COLOUR('',#18318);
#18320=FILL_AREA_STYLE('',(#18319));
#18321=SURFACE_STYLE_FILL_AREA(#18320);
#18322=SURFACE_SIDE_STYLE('',(#18321));
#18323=SURFACE_STYLE_USAGE(.BOTH.,#18322);
#18324=PRESENTATION_STYLE_ASSIGNMENT((#18323));
ENDSEC;
END-ISO-10303-21;
